ISO-10303-21;
HEADER;
/* Generated by software containing ST-Developer
 * from STEP Tools, Inc. (www.steptools.com) 
 */

FILE_DESCRIPTION(
/* description */ ('Belt tensioner idler arm'),
/* implementation_level */ '2;1');

FILE_NAME(
/* name */ 'M4x10 Cap Screw.step',
/* time_stamp */ '2026-10-28T03:22:15-07:00',
/* author */ (''),
/* organization */ (''),
/* preprocessor_version */ 'ST-DEVELOPER v20.2',
/* originating_system */ 'Autodesk Translation Framework v15.17.0.0',
/* authorisation */ '');

FILE_SCHEMA (('AUTOMOTIVE_DESIGN { 1 0 10303 214 3 1 1 }'));
ENDSEC;

DATA;
#10=MECHANICAL_DESIGN_GEOMETRIC_PRESENTATION_REPRESENTATION('',(#488),#12779);
#288=ORIENTED_CLOSED_SHELL('',*,#6225,.F.);
#292=BREP_WITH_VOIDS('Body1',#6226,(#288));
#312=CONICAL_SURFACE('',#7409,0.325,0.785398163397448);
#313=CONICAL_SURFACE('',#7413,0.335,0.785398163397448);
#314=CONICAL_SURFACE('',#7417,0.21,0.463647609000806);
#412=SHAPE_REPRESENTATION_RELATIONSHIP('SRR','None',#12961,#446);
#446=ADVANCED_BREP_SHAPE_REPRESENTATION('',(#292),#12778);
#488=STYLED_ITEM('',(#13191),#292);
#662=FACE_BOUND('',#1704,.T.);
#826=PLANE('',#7397);
#827=PLANE('',#7398);
#828=PLANE('',#7399);
#829=PLANE('',#7400);
#830=PLANE('',#7401);
#831=PLANE('',#7402);
#832=PLANE('',#7403);
#833=PLANE('',#7404);
#834=PLANE('',#7405);
#835=PLANE('',#7407);
#836=PLANE('',#7415);
#1188=FACE_OUTER_BOUND('',#1690,.T.);
#1189=FACE_OUTER_BOUND('',#1691,.T.);
#1190=FACE_OUTER_BOUND('',#1692,.T.);
#1191=FACE_OUTER_BOUND('',#1693,.T.);
#1192=FACE_OUTER_BOUND('',#1694,.T.);
#1193=FACE_OUTER_BOUND('',#1695,.T.);
#1194=FACE_OUTER_BOUND('',#1696,.T.);
#1195=FACE_OUTER_BOUND('',#1697,.T.);
#1196=FACE_OUTER_BOUND('',#1698,.T.);
#1197=FACE_OUTER_BOUND('',#1699,.T.);
#1198=FACE_OUTER_BOUND('',#1700,.T.);
#1199=FACE_OUTER_BOUND('',#1701,.T.);
#1200=FACE_OUTER_BOUND('',#1702,.T.);
#1201=FACE_OUTER_BOUND('',#1703,.T.);
#1202=FACE_OUTER_BOUND('',#1705,.T.);
#1203=FACE_OUTER_BOUND('',#1706,.T.);
#1690=EDGE_LOOP('',(#5602,#5603,#5604,#5605));
#1691=EDGE_LOOP('',(#5606,#5607,#5608,#5609));
#1692=EDGE_LOOP('',(#5610,#5611,#5612,#5613));
#1693=EDGE_LOOP('',(#5614,#5615,#5616,#5617));
#1694=EDGE_LOOP('',(#5618,#5619,#5620,#5621));
#1695=EDGE_LOOP('',(#5622,#5623,#5624,#5625));
#1696=EDGE_LOOP('',(#5626,#5627,#5628,#5629,#5630,#5631));
#1697=EDGE_LOOP('',(#5632,#5633,#5634,#5635,#5636,#5637));
#1698=EDGE_LOOP('',(#5638));
#1699=EDGE_LOOP('',(#5639));
#1700=EDGE_LOOP('',(#5640,#5641,#5642,#5643));
#1701=EDGE_LOOP('',(#5644,#5645,#5646,#5647));
#1702=EDGE_LOOP('',(#5648,#5649,#5650,#5651));
#1703=EDGE_LOOP('',(#5652));
#1704=EDGE_LOOP('',(#5653));
#1705=EDGE_LOOP('',(#5654,#5655,#5656,#5657));
#1706=EDGE_LOOP('',(#5658,#5659,#5660,#5661));
#2033=LINE('',#12625,#2382);
#2034=LINE('',#12627,#2383);
#2035=LINE('',#12629,#2384);
#2036=LINE('',#12630,#2385);
#2037=LINE('',#12633,#2386);
#2038=LINE('',#12635,#2387);
#2039=LINE('',#12636,#2388);
#2040=LINE('',#12639,#2389);
#2041=LINE('',#12641,#2390);
#2042=LINE('',#12642,#2391);
#2043=LINE('',#12645,#2392);
#2044=LINE('',#12647,#2393);
#2045=LINE('',#12648,#2394);
#2046=LINE('',#12651,#2395);
#2047=LINE('',#12653,#2396);
#2048=LINE('',#12654,#2397);
#2049=LINE('',#12656,#2398);
#2050=LINE('',#12657,#2399);
#2051=LINE('',#12669,#2400);
#2052=LINE('',#12673,#2401);
#2053=LINE('',#12677,#2402);
#2054=LINE('',#12684,#2403);
#2055=LINE('',#12686,#2404);
#2382=VECTOR('',#9351,1.);
#2383=VECTOR('',#9352,1.);
#2384=VECTOR('',#9353,1.);
#2385=VECTOR('',#9354,1.);
#2386=VECTOR('',#9357,1.);
#2387=VECTOR('',#9358,1.);
#2388=VECTOR('',#9359,1.);
#2389=VECTOR('',#9362,1.);
#2390=VECTOR('',#9363,1.);
#2391=VECTOR('',#9364,1.);
#2392=VECTOR('',#9367,1.);
#2393=VECTOR('',#9368,1.);
#2394=VECTOR('',#9369,1.);
#2395=VECTOR('',#9372,1.);
#2396=VECTOR('',#9373,1.);
#2397=VECTOR('',#9374,1.);
#2398=VECTOR('',#9377,1.);
#2399=VECTOR('',#9378,1.);
#2400=VECTOR('',#9395,0.325);
#2401=VECTOR('',#9400,0.35);
#2402=VECTOR('',#9405,0.335);
#2403=VECTOR('',#9414,0.21);
#2404=VECTOR('',#9417,0.2);
#2762=CIRCLE('',#7406,0.1954);
#2763=CIRCLE('',#7408,0.3);
#2764=CIRCLE('',#7410,0.35);
#2765=CIRCLE('',#7412,0.35);
#2766=CIRCLE('',#7414,0.32);
#2767=CIRCLE('',#7416,0.22);
#2768=CIRCLE('',#7418,0.1954);
#3279=VERTEX_POINT('',#12623);
#3280=VERTEX_POINT('',#12624);
#3281=VERTEX_POINT('',#12626);
#3282=VERTEX_POINT('',#12628);
#3283=VERTEX_POINT('',#12632);
#3284=VERTEX_POINT('',#12634);
#3285=VERTEX_POINT('',#12638);
#3286=VERTEX_POINT('',#12640);
#3287=VERTEX_POINT('',#12644);
#3288=VERTEX_POINT('',#12646);
#3289=VERTEX_POINT('',#12650);
#3290=VERTEX_POINT('',#12652);
#3291=VERTEX_POINT('',#12661);
#3292=VERTEX_POINT('',#12664);
#3293=VERTEX_POINT('',#12667);
#3294=VERTEX_POINT('',#12671);
#3295=VERTEX_POINT('',#12675);
#3296=VERTEX_POINT('',#12679);
#3297=VERTEX_POINT('',#12682);
#4056=EDGE_CURVE('',#3279,#3280,#2033,.T.);
#4057=EDGE_CURVE('',#3280,#3281,#2034,.T.);
#4058=EDGE_CURVE('',#3281,#3282,#2035,.T.);
#4059=EDGE_CURVE('',#3279,#3282,#2036,.T.);
#4060=EDGE_CURVE('',#3280,#3283,#2037,.T.);
#4061=EDGE_CURVE('',#3283,#3284,#2038,.T.);
#4062=EDGE_CURVE('',#3284,#3281,#2039,.T.);
#4063=EDGE_CURVE('',#3283,#3285,#2040,.T.);
#4064=EDGE_CURVE('',#3285,#3286,#2041,.T.);
#4065=EDGE_CURVE('',#3286,#3284,#2042,.T.);
#4066=EDGE_CURVE('',#3285,#3287,#2043,.T.);
#4067=EDGE_CURVE('',#3287,#3288,#2044,.T.);
#4068=EDGE_CURVE('',#3288,#3286,#2045,.T.);
#4069=EDGE_CURVE('',#3287,#3289,#2046,.T.);
#4070=EDGE_CURVE('',#3289,#3290,#2047,.T.);
#4071=EDGE_CURVE('',#3290,#3288,#2048,.T.);
#4072=EDGE_CURVE('',#3289,#3279,#2049,.T.);
#4073=EDGE_CURVE('',#3282,#3290,#2050,.T.);
#4074=EDGE_CURVE('',#3291,#3291,#2762,.T.);
#4075=EDGE_CURVE('',#3292,#3292,#2763,.T.);
#4076=EDGE_CURVE('',#3293,#3293,#2764,.T.);
#4077=EDGE_CURVE('',#3293,#3292,#2051,.T.);
#4078=EDGE_CURVE('',#3294,#3294,#2765,.T.);
#4079=EDGE_CURVE('',#3294,#3293,#2052,.T.);
#4080=EDGE_CURVE('',#3295,#3295,#2766,.T.);
#4081=EDGE_CURVE('',#3295,#3294,#2053,.T.);
#4082=EDGE_CURVE('',#3296,#3296,#2767,.T.);
#4083=EDGE_CURVE('',#3297,#3297,#2768,.F.);
#4084=EDGE_CURVE('',#3297,#3296,#2054,.T.);
#4085=EDGE_CURVE('',#3291,#3297,#2055,.T.);
#5602=ORIENTED_EDGE('',*,*,#4056,.T.);
#5603=ORIENTED_EDGE('',*,*,#4057,.T.);
#5604=ORIENTED_EDGE('',*,*,#4058,.T.);
#5605=ORIENTED_EDGE('',*,*,#4059,.F.);
#5606=ORIENTED_EDGE('',*,*,#4060,.T.);
#5607=ORIENTED_EDGE('',*,*,#4061,.T.);
#5608=ORIENTED_EDGE('',*,*,#4062,.T.);
#5609=ORIENTED_EDGE('',*,*,#4057,.F.);
#5610=ORIENTED_EDGE('',*,*,#4063,.T.);
#5611=ORIENTED_EDGE('',*,*,#4064,.T.);
#5612=ORIENTED_EDGE('',*,*,#4065,.T.);
#5613=ORIENTED_EDGE('',*,*,#4061,.F.);
#5614=ORIENTED_EDGE('',*,*,#4066,.T.);
#5615=ORIENTED_EDGE('',*,*,#4067,.T.);
#5616=ORIENTED_EDGE('',*,*,#4068,.T.);
#5617=ORIENTED_EDGE('',*,*,#4064,.F.);
#5618=ORIENTED_EDGE('',*,*,#4069,.T.);
#5619=ORIENTED_EDGE('',*,*,#4070,.T.);
#5620=ORIENTED_EDGE('',*,*,#4071,.T.);
#5621=ORIENTED_EDGE('',*,*,#4067,.F.);
#5622=ORIENTED_EDGE('',*,*,#4072,.T.);
#5623=ORIENTED_EDGE('',*,*,#4059,.T.);
#5624=ORIENTED_EDGE('',*,*,#4073,.T.);
#5625=ORIENTED_EDGE('',*,*,#4070,.F.);
#5626=ORIENTED_EDGE('',*,*,#4072,.F.);
#5627=ORIENTED_EDGE('',*,*,#4069,.F.);
#5628=ORIENTED_EDGE('',*,*,#4066,.F.);
#5629=ORIENTED_EDGE('',*,*,#4063,.F.);
#5630=ORIENTED_EDGE('',*,*,#4060,.F.);
#5631=ORIENTED_EDGE('',*,*,#4056,.F.);
#5632=ORIENTED_EDGE('',*,*,#4073,.F.);
#5633=ORIENTED_EDGE('',*,*,#4058,.F.);
#5634=ORIENTED_EDGE('',*,*,#4062,.F.);
#5635=ORIENTED_EDGE('',*,*,#4065,.F.);
#5636=ORIENTED_EDGE('',*,*,#4068,.F.);
#5637=ORIENTED_EDGE('',*,*,#4071,.F.);
#5638=ORIENTED_EDGE('',*,*,#4074,.F.);
#5639=ORIENTED_EDGE('',*,*,#4075,.F.);
#5640=ORIENTED_EDGE('',*,*,#4076,.F.);
#5641=ORIENTED_EDGE('',*,*,#4077,.T.);
#5642=ORIENTED_EDGE('',*,*,#4075,.T.);
#5643=ORIENTED_EDGE('',*,*,#4077,.F.);
#5644=ORIENTED_EDGE('',*,*,#4078,.F.);
#5645=ORIENTED_EDGE('',*,*,#4079,.T.);
#5646=ORIENTED_EDGE('',*,*,#4076,.T.);
#5647=ORIENTED_EDGE('',*,*,#4079,.F.);
#5648=ORIENTED_EDGE('',*,*,#4080,.F.);
#5649=ORIENTED_EDGE('',*,*,#4081,.T.);
#5650=ORIENTED_EDGE('',*,*,#4078,.T.);
#5651=ORIENTED_EDGE('',*,*,#4081,.F.);
#5652=ORIENTED_EDGE('',*,*,#4080,.T.);
#5653=ORIENTED_EDGE('',*,*,#4082,.F.);
#5654=ORIENTED_EDGE('',*,*,#4083,.F.);
#5655=ORIENTED_EDGE('',*,*,#4084,.T.);
#5656=ORIENTED_EDGE('',*,*,#4082,.T.);
#5657=ORIENTED_EDGE('',*,*,#4084,.F.);
#5658=ORIENTED_EDGE('',*,*,#4074,.T.);
#5659=ORIENTED_EDGE('',*,*,#4085,.T.);
#5660=ORIENTED_EDGE('',*,*,#4083,.T.);
#5661=ORIENTED_EDGE('',*,*,#4085,.F.);
#5812=CYLINDRICAL_SURFACE('',#7411,0.35);
#5813=CYLINDRICAL_SURFACE('',#7419,0.1954);
#6165=ADVANCED_FACE('',(#1188),#826,.F.);
#6166=ADVANCED_FACE('',(#1189),#827,.F.);
#6167=ADVANCED_FACE('',(#1190),#828,.F.);
#6168=ADVANCED_FACE('',(#1191),#829,.F.);
#6169=ADVANCED_FACE('',(#1192),#830,.F.);
#6170=ADVANCED_FACE('',(#1193),#831,.F.);
#6171=ADVANCED_FACE('',(#1194),#832,.F.);
#6172=ADVANCED_FACE('',(#1195),#833,.F.);
#6173=ADVANCED_FACE('',(#1196),#834,.F.);
#6174=ADVANCED_FACE('',(#1197),#835,.T.);
#6175=ADVANCED_FACE('',(#1198),#312,.T.);
#6176=ADVANCED_FACE('',(#1199),#5812,.T.);
#6177=ADVANCED_FACE('',(#1200),#313,.T.);
#6178=ADVANCED_FACE('',(#1201,#662),#836,.T.);
#6179=ADVANCED_FACE('',(#1202),#314,.T.);
#6180=ADVANCED_FACE('',(#1203),#5813,.T.);
#6225=CLOSED_SHELL('',(#6165,#6166,#6167,#6168,#6169,#6170,#6171,#6172));
#6226=CLOSED_SHELL('',(#6173,#6174,#6175,#6176,#6177,#6178,#6179,#6180));
#7396=AXIS2_PLACEMENT_3D('',#12621,#9347,#9348);
#7397=AXIS2_PLACEMENT_3D('',#12622,#9349,#9350);
#7398=AXIS2_PLACEMENT_3D('',#12631,#9355,#9356);
#7399=AXIS2_PLACEMENT_3D('',#12637,#9360,#9361);
#7400=AXIS2_PLACEMENT_3D('',#12643,#9365,#9366);
#7401=AXIS2_PLACEMENT_3D('',#12649,#9370,#9371);
#7402=AXIS2_PLACEMENT_3D('',#12655,#9375,#9376);
#7403=AXIS2_PLACEMENT_3D('',#12658,#9379,#9380);
#7404=AXIS2_PLACEMENT_3D('',#12659,#9381,#9382);
#7405=AXIS2_PLACEMENT_3D('',#12660,#9383,#9384);
#7406=AXIS2_PLACEMENT_3D('',#12662,#9385,#9386);
#7407=AXIS2_PLACEMENT_3D('',#12663,#9387,#9388);
#7408=AXIS2_PLACEMENT_3D('',#12665,#9389,#9390);
#7409=AXIS2_PLACEMENT_3D('',#12666,#9391,#9392);
#7410=AXIS2_PLACEMENT_3D('',#12668,#9393,#9394);
#7411=AXIS2_PLACEMENT_3D('',#12670,#9396,#9397);
#7412=AXIS2_PLACEMENT_3D('',#12672,#9398,#9399);
#7413=AXIS2_PLACEMENT_3D('',#12674,#9401,#9402);
#7414=AXIS2_PLACEMENT_3D('',#12676,#9403,#9404);
#7415=AXIS2_PLACEMENT_3D('',#12678,#9406,#9407);
#7416=AXIS2_PLACEMENT_3D('',#12680,#9408,#9409);
#7417=AXIS2_PLACEMENT_3D('',#12681,#9410,#9411);
#7418=AXIS2_PLACEMENT_3D('',#12683,#9412,#9413);
#7419=AXIS2_PLACEMENT_3D('',#12685,#9415,#9416);
#9347=DIRECTION('axis',(0.,0.,1.));
#9348=DIRECTION('refdir',(1.,0.,0.));
#9349=DIRECTION('center_axis',(0.866025403784439,0.,-0.5));
#9350=DIRECTION('ref_axis',(0.5,0.,0.866025403784439));
#9351=DIRECTION('',(-0.5,0.,-0.866025403784439));
#9352=DIRECTION('',(0.,-1.,0.));
#9353=DIRECTION('',(0.5,0.,0.866025403784439));
#9354=DIRECTION('',(0.,-1.,0.));
#9355=DIRECTION('center_axis',(1.60246890531964E-16,0.,-1.));
#9356=DIRECTION('ref_axis',(1.,0.,1.60246890531964E-16));
#9357=DIRECTION('',(-1.,0.,-1.60246890531964E-16));
#9358=DIRECTION('',(0.,-1.,0.));
#9359=DIRECTION('',(1.,0.,1.60246890531964E-16));
#9360=DIRECTION('center_axis',(-0.866025403784439,0.,-0.5));
#9361=DIRECTION('ref_axis',(0.5,0.,-0.866025403784439));
#9362=DIRECTION('',(-0.5,0.,0.866025403784439));
#9363=DIRECTION('',(0.,-1.,0.));
#9364=DIRECTION('',(0.5,0.,-0.866025403784439));
#9365=DIRECTION('center_axis',(-0.866025403784439,0.,0.5));
#9366=DIRECTION('ref_axis',(-0.5,0.,-0.866025403784439));
#9367=DIRECTION('',(0.5,0.,0.866025403784439));
#9368=DIRECTION('',(0.,-1.,0.));
#9369=DIRECTION('',(-0.5,0.,-0.866025403784439));
#9370=DIRECTION('center_axis',(-1.60246890531964E-16,0.,1.));
#9371=DIRECTION('ref_axis',(-1.,0.,-1.60246890531964E-16));
#9372=DIRECTION('',(1.,0.,1.60246890531964E-16));
#9373=DIRECTION('',(0.,-1.,0.));
#9374=DIRECTION('',(-1.,0.,-1.60246890531964E-16));
#9375=DIRECTION('center_axis',(0.866025403784439,0.,0.5));
#9376=DIRECTION('ref_axis',(-0.5,0.,0.866025403784439));
#9377=DIRECTION('',(0.5,0.,-0.866025403784439));
#9378=DIRECTION('',(-0.5,0.,0.866025403784439));
#9379=DIRECTION('center_axis',(0.,1.,0.));
#9380=DIRECTION('ref_axis',(1.,0.,0.));
#9381=DIRECTION('center_axis',(0.,-1.,0.));
#9382=DIRECTION('ref_axis',(0.,0.,-1.));
#9383=DIRECTION('center_axis',(0.,1.,0.));
#9384=DIRECTION('ref_axis',(1.,0.,0.));
#9385=DIRECTION('center_axis',(0.,1.,0.));
#9386=DIRECTION('ref_axis',(1.,0.,0.));
#9387=DIRECTION('center_axis',(0.,1.,0.));
#9388=DIRECTION('ref_axis',(0.,0.,1.));
#9389=DIRECTION('center_axis',(0.,-1.,0.));
#9390=DIRECTION('ref_axis',(1.,0.,0.));
#9391=DIRECTION('center_axis',(0.,-1.,0.));
#9392=DIRECTION('ref_axis',(1.,0.,0.));
#9393=DIRECTION('center_axis',(0.,-1.,0.));
#9394=DIRECTION('ref_axis',(1.,0.,0.));
#9395=DIRECTION('',(0.707106781186547,0.707106781186548,8.65956056235493E-17));
#9396=DIRECTION('center_axis',(0.,-1.,0.));
#9397=DIRECTION('ref_axis',(1.,0.,0.));
#9398=DIRECTION('center_axis',(0.,-1.,0.));
#9399=DIRECTION('ref_axis',(1.,0.,0.));
#9400=DIRECTION('',(0.,1.,0.));
#9401=DIRECTION('center_axis',(0.,1.,0.));
#9402=DIRECTION('ref_axis',(1.,0.,0.));
#9403=DIRECTION('center_axis',(0.,-1.,0.));
#9404=DIRECTION('ref_axis',(1.,0.,0.));
#9405=DIRECTION('',(-0.707106781186547,0.707106781186548,-8.65956056235493E-17));
#9406=DIRECTION('center_axis',(0.,-1.,0.));
#9407=DIRECTION('ref_axis',(0.,0.,-1.));
#9408=DIRECTION('center_axis',(0.,-1.,0.));
#9409=DIRECTION('ref_axis',(1.,0.,0.));
#9410=DIRECTION('center_axis',(0.,1.,0.));
#9411=DIRECTION('ref_axis',(1.,0.,0.));
#9412=DIRECTION('center_axis',(0.,1.,0.));
#9413=DIRECTION('ref_axis',(1.,0.,0.));
#9414=DIRECTION('',(-0.447213595499958,0.894427190999916,-5.47678698264203E-17));
#9415=DIRECTION('center_axis',(0.,-1.,0.));
#9416=DIRECTION('ref_axis',(1.,0.,0.));
#9417=DIRECTION('',(0.,1.,0.));
#12621=CARTESIAN_POINT('',(0.,0.,0.));
#12622=CARTESIAN_POINT('Origin',(0.0866025403784439,-0.4,-0.15));
#12623=CARTESIAN_POINT('',(0.173205080756888,-0.4,0.));
#12624=CARTESIAN_POINT('',(0.0866025403784439,-0.4,-0.15));
#12625=CARTESIAN_POINT('',(0.173205080756888,-0.4,0.));
#12626=CARTESIAN_POINT('',(0.0866025403784439,-0.64,-0.15));
#12627=CARTESIAN_POINT('',(0.0866025403784439,-0.4,-0.15));
#12628=CARTESIAN_POINT('',(0.173205080756888,-0.64,0.));
#12629=CARTESIAN_POINT('',(0.173205080756888,-0.64,0.));
#12630=CARTESIAN_POINT('',(0.173205080756888,-0.4,0.));
#12631=CARTESIAN_POINT('Origin',(-0.0866025403784438,-0.4,-0.15));
#12632=CARTESIAN_POINT('',(-0.0866025403784438,-0.4,-0.15));
#12633=CARTESIAN_POINT('',(0.0866025403784439,-0.4,-0.15));
#12634=CARTESIAN_POINT('',(-0.0866025403784438,-0.64,-0.15));
#12635=CARTESIAN_POINT('',(-0.0866025403784438,-0.4,-0.15));
#12636=CARTESIAN_POINT('',(0.0866025403784439,-0.64,-0.15));
#12637=CARTESIAN_POINT('Origin',(-0.173205080756888,-0.4,-2.77555756156289E-17));
#12638=CARTESIAN_POINT('',(-0.173205080756888,-0.4,-2.12115047744981E-17));
#12639=CARTESIAN_POINT('',(-0.0866025403784438,-0.4,-0.15));
#12640=CARTESIAN_POINT('',(-0.173205080756888,-0.64,-2.77555756156289E-17));
#12641=CARTESIAN_POINT('',(-0.173205080756888,-0.4,-2.12115047744981E-17));
#12642=CARTESIAN_POINT('',(-0.0866025403784438,-0.64,-0.15));
#12643=CARTESIAN_POINT('Origin',(-0.0866025403784439,-0.4,0.15));
#12644=CARTESIAN_POINT('',(-0.0866025403784439,-0.4,0.15));
#12645=CARTESIAN_POINT('',(-0.173205080756888,-0.4,-2.12115047744981E-17));
#12646=CARTESIAN_POINT('',(-0.0866025403784439,-0.64,0.15));
#12647=CARTESIAN_POINT('',(-0.0866025403784439,-0.4,0.15));
#12648=CARTESIAN_POINT('',(-0.173205080756888,-0.64,-2.12115047744981E-17));
#12649=CARTESIAN_POINT('Origin',(0.0866025403784439,-0.4,0.15));
#12650=CARTESIAN_POINT('',(0.0866025403784439,-0.4,0.15));
#12651=CARTESIAN_POINT('',(-0.0866025403784439,-0.4,0.15));
#12652=CARTESIAN_POINT('',(0.0866025403784439,-0.64,0.15));
#12653=CARTESIAN_POINT('',(0.0866025403784439,-0.4,0.15));
#12654=CARTESIAN_POINT('',(-0.0866025403784439,-0.64,0.15));
#12655=CARTESIAN_POINT('Origin',(0.173205080756888,-0.4,0.));
#12656=CARTESIAN_POINT('',(0.0866025403784439,-0.4,0.15));
#12657=CARTESIAN_POINT('',(0.0866025403784439,-0.64,0.15));
#12658=CARTESIAN_POINT('Origin',(0.,-0.4,-2.77555756156289E-17));
#12659=CARTESIAN_POINT('Origin',(0.,-0.64,-2.77555756156289E-17));
#12660=CARTESIAN_POINT('Origin',(0.,-1.,0.));
#12661=CARTESIAN_POINT('',(-0.1954,-1.,2.39295984553393E-17));
#12662=CARTESIAN_POINT('Origin',(0.,-1.,0.));
#12663=CARTESIAN_POINT('Origin',(0.3,0.4,0.));
#12664=CARTESIAN_POINT('',(-0.3,0.4,-3.67394039744206E-17));
#12665=CARTESIAN_POINT('Origin',(0.,0.4,0.));
#12666=CARTESIAN_POINT('Origin',(0.,0.375,0.));
#12667=CARTESIAN_POINT('',(-0.35,0.35,-4.28626379701573E-17));
#12668=CARTESIAN_POINT('Origin',(0.,0.35,0.));
#12669=CARTESIAN_POINT('',(-0.325,0.375,-3.9801020972289E-17));
#12670=CARTESIAN_POINT('Origin',(0.,0.19,0.));
#12671=CARTESIAN_POINT('',(-0.35,0.03,-4.28626379701574E-17));
#12672=CARTESIAN_POINT('Origin',(0.,0.03,0.));
#12673=CARTESIAN_POINT('',(-0.35,0.19,-4.28626379701574E-17));
#12674=CARTESIAN_POINT('Origin',(0.,0.0149999999999999,0.));
#12675=CARTESIAN_POINT('',(-0.32,-3.29597460435593E-17,-3.91886975727153E-17));
#12676=CARTESIAN_POINT('Origin',(0.,0.,0.));
#12677=CARTESIAN_POINT('',(-0.335,0.0149999999999999,-4.10256677714363E-17));
#12678=CARTESIAN_POINT('Origin',(0.22,0.,0.));
#12679=CARTESIAN_POINT('',(-0.22,-6.93889390390723E-18,-2.69422295812418E-17));
#12680=CARTESIAN_POINT('Origin',(0.,0.,0.));
#12681=CARTESIAN_POINT('Origin',(0.,-0.02,0.));
#12682=CARTESIAN_POINT('',(-0.1954,-0.0492,2.39295984553393E-17));
#12683=CARTESIAN_POINT('Origin',(0.,-0.0492,0.));
#12684=CARTESIAN_POINT('',(-0.21,-0.02,-2.57175827820944E-17));
#12685=CARTESIAN_POINT('Origin',(0.,-0.8,0.));
#12686=CARTESIAN_POINT('',(-0.1954,-0.8,-2.39295984553393E-17));
#12738=UNCERTAINTY_MEASURE_WITH_UNIT(LENGTH_MEASURE(0.001),#12780,
'DISTANCE_ACCURACY_VALUE',
'Maximum model space distance between geometric entities at asserted c
onnectivities');
#12739=UNCERTAINTY_MEASURE_WITH_UNIT(LENGTH_MEASURE(0.001),#12780,
'DISTANCE_ACCURACY_VALUE',
'Maximum model space distance between geometric entities at asserted c
onnectivities');
#12778=(
GEOMETRIC_REPRESENTATION_CONTEXT(3)
GLOBAL_UNCERTAINTY_ASSIGNED_CONTEXT((#12738))
GLOBAL_UNIT_ASSIGNED_CONTEXT((#12780,#12782,#12783))
REPRESENTATION_CONTEXT('','3D')
);
#12779=(
GEOMETRIC_REPRESENTATION_CONTEXT(3)
GLOBAL_UNCERTAINTY_ASSIGNED_CONTEXT((#12739))
GLOBAL_UNIT_ASSIGNED_CONTEXT((#12780,#12782,#12783))
REPRESENTATION_CONTEXT('','3D')
);
#12780=(
LENGTH_UNIT()
NAMED_UNIT(*)
SI_UNIT(.CENTI.,.METRE.)
);
#12782=(
NAMED_UNIT(*)
PLANE_ANGLE_UNIT()
SI_UNIT($,.RADIAN.)
);
#12783=(
NAMED_UNIT(*)
SI_UNIT($,.STERADIAN.)
SOLID_ANGLE_UNIT()
);
#12822=SHAPE_DEFINITION_REPRESENTATION(#12909,#12961);
#12909=PRODUCT_DEFINITION_SHAPE('',$,#13001);
#12961=SHAPE_REPRESENTATION('',(#7396),#12778);
#12962=PRODUCT_DEFINITION_CONTEXT('part definition',#13081,'design');
#13001=PRODUCT_DEFINITION('M4x10 Cap Screw','M4x10 Cap Screw',#13040,#12962);
#13040=PRODUCT_DEFINITION_FORMATION('',$,#13121);
#13081=APPLICATION_CONTEXT(
'Core Data for Automotive Mechanical Design Process');
#13082=PRODUCT_CONTEXT('part definition',#13081,'mechanical');
#13121=PRODUCT('M4x10 Cap Screw','M4x10 Cap Screw','M4x10 Cap Screw',(#13082));
#13185=COLOUR_RGB('Black',0.12,0.14,0.17);
#13186=FILL_AREA_STYLE_COLOUR('',#13185);
#13187=FILL_AREA_STYLE('',(#13186));
#13188=SURFACE_STYLE_FILL_AREA(#13187);
#13189=SURFACE_SIDE_STYLE('',(#13188));
#13190=SURFACE_STYLE_USAGE(.BOTH.,#13189);
#13191=PRESENTATION_STYLE_ASSIGNMENT((#13190));
ENDSEC;
END-ISO-10303-21;
